ISO-10303-21;
HEADER;
/* Generated by software containing ST-Developer
 * from STEP Tools, Inc. (www.steptools.com) 
 */

FILE_DESCRIPTION(
/* description */ ('Bearing friction torque test rig'),
/* implementation_level */ '2;1');

FILE_NAME(
/* name */ 'Journal collar (1).step',
/* time_stamp */ '2026-10-28T03:24:04-07:00',
/* author */ (''),
/* organization */ (''),
/* preprocessor_version */ 'ST-DEVELOPER v20.2',
/* originating_system */ 'Autodesk Translation Framework v15.17.0.0',
/* authorisation */ '');

FILE_SCHEMA (('AUTOMOTIVE_DESIGN { 1 0 10303 214 3 1 1 }'));
ENDSEC;

DATA;
#10=MECHANICAL_DESIGN_GEOMETRIC_PRESENTATION_REPRESENTATION('',(#586),#14822);
#379=B_SPLINE_CURVE_WITH_KNOTS('',3,(#14245,#14246,#14247,#14248,#14249,
#14250,#14251,#14252,#14253,#14254),.UNSPECIFIED.,.F.,.F.,(4,2,2,2,4),(0.818088904349175,
0.878131747417166,0.957937926194037,1.03774410497091,1.0977869480389),
 .UNSPECIFIED.);
#380=B_SPLINE_CURVE_WITH_KNOTS('',3,(#14260,#14261,#14262,#14263,#14264,
#14265,#14266,#14267,#14268,#14269,#14270,#14271,#14272,#14273,#14274,#14275,
#14276,#14277),.UNSPECIFIED.,.F.,.F.,(4,2,2,2,2,2,2,2,4),(0.,0.0793616477694787,
0.158723295538957,0.238079516586307,0.317435737633657,0.396791958681006,
0.476148179728356,0.555509827497835,0.634871475267313),.UNSPECIFIED.);
#381=B_SPLINE_CURVE_WITH_KNOTS('',3,(#14278,#14279,#14280,#14281,#14282,
#14283,#14284,#14285,#14286,#14287,#14288,#14289,#14290,#14291,#14292,#14293,
#14294,#14295),.UNSPECIFIED.,.F.,.F.,(4,2,2,2,2,2,2,2,4),(0.634871475267313,
0.714233123036792,0.793594770806271,0.87295099185362,0.95230721290097,1.03166343394832,
1.11101965499567,1.19038130276515,1.26974295053463),.UNSPECIFIED.);
#382=B_SPLINE_CURVE_WITH_KNOTS('',3,(#14298,#14299,#14300,#14301,#14302,
#14303,#14304,#14305,#14306,#14307),.UNSPECIFIED.,.F.,.F.,(4,2,2,2,4),(0.179463620219817,
0.239506463287808,0.319312642064679,0.39911882084155,0.459161663909542),
 .UNSPECIFIED.);
#493=SHAPE_REPRESENTATION_RELATIONSHIP('SRR','None',#15035,#532);
#532=ADVANCED_BREP_SHAPE_REPRESENTATION('',(#637),#14815);
#586=STYLED_ITEM('',(#15277),#637);
#637=MANIFOLD_SOLID_BREP('Body1',#7705);
#844=FACE_BOUND('',#2139,.T.);
#845=FACE_BOUND('',#2141,.T.);
#846=FACE_BOUND('',#2143,.T.);
#847=FACE_BOUND('',#2145,.T.);
#1069=PLANE('',#9039);
#1070=PLANE('',#9044);
#1071=PLANE('',#9051);
#1072=PLANE('',#9052);
#1490=FACE_OUTER_BOUND('',#2135,.T.);
#1491=FACE_OUTER_BOUND('',#2136,.T.);
#1492=FACE_OUTER_BOUND('',#2137,.T.);
#1493=FACE_OUTER_BOUND('',#2138,.T.);
#1494=FACE_OUTER_BOUND('',#2140,.T.);
#1495=FACE_OUTER_BOUND('',#2142,.T.);
#1496=FACE_OUTER_BOUND('',#2144,.T.);
#2135=EDGE_LOOP('',(#6812,#6813));
#2136=EDGE_LOOP('',(#6814,#6815,#6816,#6817,#6818,#6819,#6820,#6821,#6822));
#2137=EDGE_LOOP('',(#6823,#6824,#6825));
#2138=EDGE_LOOP('',(#6826,#6827,#6828,#6829));
#2139=EDGE_LOOP('',(#6830,#6831,#6832,#6833));
#2140=EDGE_LOOP('',(#6834,#6835,#6836,#6837));
#2141=EDGE_LOOP('',(#6838,#6839));
#2142=EDGE_LOOP('',(#6840));
#2143=EDGE_LOOP('',(#6841));
#2144=EDGE_LOOP('',(#6842));
#2145=EDGE_LOOP('',(#6843));
#2613=LINE('',#14241,#3057);
#2614=LINE('',#14258,#3058);
#2615=LINE('',#14309,#3059);
#2616=LINE('',#14314,#3060);
#2617=LINE('',#14320,#3061);
#3057=VECTOR('',#11356,1.);
#3058=VECTOR('',#11363,0.21);
#3059=VECTOR('',#11368,1.);
#3060=VECTOR('',#11373,0.605);
#3061=VECTOR('',#11380,1.);
#3503=CIRCLE('',#9040,0.21);
#3504=CIRCLE('',#9042,0.21);
#3505=CIRCLE('',#9043,0.21);
#3506=CIRCLE('',#9046,0.605);
#3507=CIRCLE('',#9047,0.605);
#3508=CIRCLE('',#9049,1.);
#3509=CIRCLE('',#9050,1.);
#4122=VERTEX_POINT('',#14239);
#4123=VERTEX_POINT('',#14240);
#4124=VERTEX_POINT('',#14244);
#4125=VERTEX_POINT('',#14255);
#4126=VERTEX_POINT('',#14257);
#4127=VERTEX_POINT('',#14259);
#4128=VERTEX_POINT('',#14296);
#4129=VERTEX_POINT('',#14311);
#4130=VERTEX_POINT('',#14313);
#4131=VERTEX_POINT('',#14317);
#4132=VERTEX_POINT('',#14319);
#5032=EDGE_CURVE('',#4122,#4123,#2613,.T.);
#5033=EDGE_CURVE('',#4122,#4123,#3503,.T.);
#5034=EDGE_CURVE('',#4124,#4122,#379,.T.);
#5035=EDGE_CURVE('',#4125,#4124,#3504,.T.);
#5036=EDGE_CURVE('',#4125,#4126,#2614,.T.);
#5037=EDGE_CURVE('',#4127,#4126,#380,.T.);
#5038=EDGE_CURVE('',#4126,#4127,#381,.T.);
#5039=EDGE_CURVE('',#4128,#4125,#3505,.T.);
#5040=EDGE_CURVE('',#4123,#4128,#382,.T.);
#5041=EDGE_CURVE('',#4128,#4124,#2615,.T.);
#5042=EDGE_CURVE('',#4129,#4129,#3506,.T.);
#5043=EDGE_CURVE('',#4129,#4130,#2616,.T.);
#5044=EDGE_CURVE('',#4130,#4130,#3507,.T.);
#5045=EDGE_CURVE('',#4131,#4131,#3508,.T.);
#5046=EDGE_CURVE('',#4131,#4132,#2617,.T.);
#5047=EDGE_CURVE('',#4132,#4132,#3509,.T.);
#6812=ORIENTED_EDGE('',*,*,#5032,.F.);
#6813=ORIENTED_EDGE('',*,*,#5033,.T.);
#6814=ORIENTED_EDGE('',*,*,#5034,.F.);
#6815=ORIENTED_EDGE('',*,*,#5035,.F.);
#6816=ORIENTED_EDGE('',*,*,#5036,.T.);
#6817=ORIENTED_EDGE('',*,*,#5037,.F.);
#6818=ORIENTED_EDGE('',*,*,#5038,.F.);
#6819=ORIENTED_EDGE('',*,*,#5036,.F.);
#6820=ORIENTED_EDGE('',*,*,#5039,.F.);
#6821=ORIENTED_EDGE('',*,*,#5040,.F.);
#6822=ORIENTED_EDGE('',*,*,#5033,.F.);
#6823=ORIENTED_EDGE('',*,*,#5041,.F.);
#6824=ORIENTED_EDGE('',*,*,#5039,.T.);
#6825=ORIENTED_EDGE('',*,*,#5035,.T.);
#6826=ORIENTED_EDGE('',*,*,#5042,.F.);
#6827=ORIENTED_EDGE('',*,*,#5043,.T.);
#6828=ORIENTED_EDGE('',*,*,#5044,.T.);
#6829=ORIENTED_EDGE('',*,*,#5043,.F.);
#6830=ORIENTED_EDGE('',*,*,#5040,.T.);
#6831=ORIENTED_EDGE('',*,*,#5041,.T.);
#6832=ORIENTED_EDGE('',*,*,#5034,.T.);
#6833=ORIENTED_EDGE('',*,*,#5032,.T.);
#6834=ORIENTED_EDGE('',*,*,#5045,.F.);
#6835=ORIENTED_EDGE('',*,*,#5046,.T.);
#6836=ORIENTED_EDGE('',*,*,#5047,.T.);
#6837=ORIENTED_EDGE('',*,*,#5046,.F.);
#6838=ORIENTED_EDGE('',*,*,#5037,.T.);
#6839=ORIENTED_EDGE('',*,*,#5038,.T.);
#6840=ORIENTED_EDGE('',*,*,#5045,.T.);
#6841=ORIENTED_EDGE('',*,*,#5042,.T.);
#6842=ORIENTED_EDGE('',*,*,#5047,.F.);
#6843=ORIENTED_EDGE('',*,*,#5044,.F.);
#7188=CYLINDRICAL_SURFACE('',#9041,0.21);
#7189=CYLINDRICAL_SURFACE('',#9045,0.605);
#7190=CYLINDRICAL_SURFACE('',#9048,1.);
#7601=ADVANCED_FACE('',(#1490),#1069,.T.);
#7602=ADVANCED_FACE('',(#1491),#7188,.F.);
#7603=ADVANCED_FACE('',(#1492),#1070,.T.);
#7604=ADVANCED_FACE('',(#1493,#844),#7189,.F.);
#7605=ADVANCED_FACE('',(#1494,#845),#7190,.T.);
#7606=ADVANCED_FACE('',(#1495,#846),#1071,.T.);
#7607=ADVANCED_FACE('',(#1496,#847),#1072,.F.);
#7705=CLOSED_SHELL('',(#7601,#7602,#7603,#7604,#7605,#7606,#7607));
#9038=AXIS2_PLACEMENT_3D('',#14237,#11352,#11353);
#9039=AXIS2_PLACEMENT_3D('',#14238,#11354,#11355);
#9040=AXIS2_PLACEMENT_3D('',#14242,#11357,#11358);
#9041=AXIS2_PLACEMENT_3D('',#14243,#11359,#11360);
#9042=AXIS2_PLACEMENT_3D('',#14256,#11361,#11362);
#9043=AXIS2_PLACEMENT_3D('',#14297,#11364,#11365);
#9044=AXIS2_PLACEMENT_3D('',#14308,#11366,#11367);
#9045=AXIS2_PLACEMENT_3D('',#14310,#11369,#11370);
#9046=AXIS2_PLACEMENT_3D('',#14312,#11371,#11372);
#9047=AXIS2_PLACEMENT_3D('',#14315,#11374,#11375);
#9048=AXIS2_PLACEMENT_3D('',#14316,#11376,#11377);
#9049=AXIS2_PLACEMENT_3D('',#14318,#11378,#11379);
#9050=AXIS2_PLACEMENT_3D('',#14321,#11381,#11382);
#9051=AXIS2_PLACEMENT_3D('',#14322,#11383,#11384);
#9052=AXIS2_PLACEMENT_3D('',#14323,#11385,#11386);
#11352=DIRECTION('axis',(0.,0.,1.));
#11353=DIRECTION('refdir',(1.,0.,0.));
#11354=DIRECTION('center_axis',(0.,0.,1.));
#11355=DIRECTION('ref_axis',(1.,0.,0.));
#11356=DIRECTION('',(0.,1.,0.));
#11357=DIRECTION('center_axis',(0.,0.,1.));
#11358=DIRECTION('ref_axis',(1.,0.,0.));
#11359=DIRECTION('center_axis',(0.,0.,1.));
#11360=DIRECTION('ref_axis',(1.,0.,0.));
#11361=DIRECTION('center_axis',(0.,0.,1.));
#11362=DIRECTION('ref_axis',(1.,0.,0.));
#11363=DIRECTION('',(0.,0.,1.));
#11364=DIRECTION('center_axis',(0.,0.,1.));
#11365=DIRECTION('ref_axis',(1.,0.,0.));
#11366=DIRECTION('center_axis',(0.,0.,1.));
#11367=DIRECTION('ref_axis',(1.,0.,0.));
#11368=DIRECTION('',(0.,-1.,0.));
#11369=DIRECTION('center_axis',(0.,1.,0.));
#11370=DIRECTION('ref_axis',(1.,0.,0.));
#11371=DIRECTION('center_axis',(0.,-1.,0.));
#11372=DIRECTION('ref_axis',(1.,0.,0.));
#11373=DIRECTION('',(0.,-1.,0.));
#11374=DIRECTION('center_axis',(0.,-1.,0.));
#11375=DIRECTION('ref_axis',(1.,0.,0.));
#11376=DIRECTION('center_axis',(0.,1.,0.));
#11377=DIRECTION('ref_axis',(1.,0.,0.));
#11378=DIRECTION('center_axis',(0.,1.,0.));
#11379=DIRECTION('ref_axis',(1.,0.,0.));
#11380=DIRECTION('',(0.,-1.,0.));
#11381=DIRECTION('center_axis',(0.,1.,0.));
#11382=DIRECTION('ref_axis',(1.,0.,0.));
#11383=DIRECTION('center_axis',(0.,1.,0.));
#11384=DIRECTION('ref_axis',(1.,0.,0.));
#11385=DIRECTION('center_axis',(0.,1.,0.));
#11386=DIRECTION('ref_axis',(1.,0.,0.));
#14237=CARTESIAN_POINT('',(0.,0.,0.));
#14238=CARTESIAN_POINT('Origin',(0.,8.6,7.59));
#14239=CARTESIAN_POINT('',(0.133884278389956,8.43821310312636,7.59));
#14240=CARTESIAN_POINT('',(0.133884278389956,8.76178689687364,7.59));
#14241=CARTESIAN_POINT('',(0.133884278389956,8.2,7.59));
#14242=CARTESIAN_POINT('Origin',(0.,8.6,7.59));
#14243=CARTESIAN_POINT('Origin',(0.,8.6,7.59));
#14244=CARTESIAN_POINT('',(-0.133884278389956,8.43821310312636,7.59));
#14245=CARTESIAN_POINT('Ctrl Pts',(-0.133884278389955,8.43821310312636,
7.59));
#14246=CARTESIAN_POINT('Ctrl Pts',(-0.1182543952608,8.42527883178237,7.59354677224418));
#14247=CARTESIAN_POINT('Ctrl Pts',(-0.100109787682298,8.41420068341256,
7.59698224789957));
#14248=CARTESIAN_POINT('Ctrl Pts',(-0.054829872132519,8.39536143894557,
7.6030741628997));
#14249=CARTESIAN_POINT('Ctrl Pts',(-0.0266020595922903,8.39,7.605));
#14250=CARTESIAN_POINT('Ctrl Pts',(0.0266020595922903,8.39,7.605));
#14251=CARTESIAN_POINT('Ctrl Pts',(0.0548298721325189,8.39536143894557,
7.6030741628997));
#14252=CARTESIAN_POINT('Ctrl Pts',(0.100109787682299,8.41420068341256,7.59698224789957));
#14253=CARTESIAN_POINT('Ctrl Pts',(0.1182543952608,8.42527883178237,7.59354677224418));
#14254=CARTESIAN_POINT('Ctrl Pts',(0.133884278389956,8.43821310312636,7.59));
#14255=CARTESIAN_POINT('',(-0.21,8.6,7.59));
#14256=CARTESIAN_POINT('Origin',(0.,8.6,7.59));
#14257=CARTESIAN_POINT('',(-0.21,8.6,7.97770138590472));
#14258=CARTESIAN_POINT('',(-0.21,8.6,7.59));
#14259=CARTESIAN_POINT('',(0.21,8.6,7.97770138590472));
#14260=CARTESIAN_POINT('Ctrl Pts',(0.21,8.6,7.97770138590472));
#14261=CARTESIAN_POINT('Ctrl Pts',(0.21,8.57354611741017,7.97770138590472));
#14262=CARTESIAN_POINT('Ctrl Pts',(0.204697017125528,8.54538474169131,7.97888646613217));
#14263=CARTESIAN_POINT('Ctrl Pts',(0.183241751515529,8.49366957869826,7.98312869991148));
#14264=CARTESIAN_POINT('Ctrl Pts',(0.167093586802906,8.47010873870456,7.98612044796649));
#14265=CARTESIAN_POINT('Ctrl Pts',(0.129892533236543,8.43290768513819,7.99170645156379));
#14266=CARTESIAN_POINT('Ctrl Pts',(0.106331154992714,8.41675852489431,7.99466914446598));
#14267=CARTESIAN_POINT('Ctrl Pts',(0.0546141143983522,8.39530253627557,
7.99884449237241));
#14268=CARTESIAN_POINT('Ctrl Pts',(0.0264520736824499,8.39,8.));
#14269=CARTESIAN_POINT('Ctrl Pts',(-0.0264520736824498,8.39,8.));
#14270=CARTESIAN_POINT('Ctrl Pts',(-0.0546141143983521,8.39530253627557,
7.99884449237241));
#14271=CARTESIAN_POINT('Ctrl Pts',(-0.106331154992714,8.41675852489431,
7.99466914446598));
#14272=CARTESIAN_POINT('Ctrl Pts',(-0.129892533236543,8.43290768513819,
7.99170645156379));
#14273=CARTESIAN_POINT('Ctrl Pts',(-0.167093586802906,8.47010873870456,
7.98612044796649));
#14274=CARTESIAN_POINT('Ctrl Pts',(-0.183241751515529,8.49366957869826,
7.98312869991148));
#14275=CARTESIAN_POINT('Ctrl Pts',(-0.204697017125528,8.54538474169131,
7.97888646613217));
#14276=CARTESIAN_POINT('Ctrl Pts',(-0.21,8.57354611741017,7.97770138590472));
#14277=CARTESIAN_POINT('Ctrl Pts',(-0.21,8.6,7.97770138590472));
#14278=CARTESIAN_POINT('Ctrl Pts',(-0.21,8.6,7.97770138590472));
#14279=CARTESIAN_POINT('Ctrl Pts',(-0.21,8.62645388258982,7.97770138590472));
#14280=CARTESIAN_POINT('Ctrl Pts',(-0.204697017125528,8.65461525830868,
7.97888646613217));
#14281=CARTESIAN_POINT('Ctrl Pts',(-0.183241751515529,8.70633042130174,
7.98312869991148));
#14282=CARTESIAN_POINT('Ctrl Pts',(-0.167093586802906,8.72989126129544,
7.98612044796649));
#14283=CARTESIAN_POINT('Ctrl Pts',(-0.129892533236543,8.76709231486181,
7.99170645156379));
#14284=CARTESIAN_POINT('Ctrl Pts',(-0.106331154992714,8.78324147510569,
7.99466914446598));
#14285=CARTESIAN_POINT('Ctrl Pts',(-0.0546141143983522,8.80469746372443,
7.99884449237241));
#14286=CARTESIAN_POINT('Ctrl Pts',(-0.0264520736824499,8.81,8.));
#14287=CARTESIAN_POINT('Ctrl Pts',(0.0264520736824499,8.81,8.));
#14288=CARTESIAN_POINT('Ctrl Pts',(0.0546141143983521,8.80469746372443,
7.99884449237241));
#14289=CARTESIAN_POINT('Ctrl Pts',(0.106331154992713,8.78324147510569,7.99466914446598));
#14290=CARTESIAN_POINT('Ctrl Pts',(0.129892533236543,8.76709231486181,7.99170645156379));
#14291=CARTESIAN_POINT('Ctrl Pts',(0.167093586802906,8.72989126129544,7.98612044796649));
#14292=CARTESIAN_POINT('Ctrl Pts',(0.183241751515529,8.70633042130174,7.98312869991148));
#14293=CARTESIAN_POINT('Ctrl Pts',(0.204697017125528,8.65461525830868,7.97888646613217));
#14294=CARTESIAN_POINT('Ctrl Pts',(0.21,8.62645388258982,7.97770138590472));
#14295=CARTESIAN_POINT('Ctrl Pts',(0.21,8.6,7.97770138590472));
#14296=CARTESIAN_POINT('',(-0.133884278389956,8.76178689687364,7.59));
#14297=CARTESIAN_POINT('Origin',(0.,8.6,7.59));
#14298=CARTESIAN_POINT('Ctrl Pts',(0.133884278389955,8.76178689687364,7.59));
#14299=CARTESIAN_POINT('Ctrl Pts',(0.1182543952608,8.77472116821763,7.59354677224418));
#14300=CARTESIAN_POINT('Ctrl Pts',(0.100109787682298,8.78579931658744,7.59698224789957));
#14301=CARTESIAN_POINT('Ctrl Pts',(0.054829872132519,8.80463856105443,7.6030741628997));
#14302=CARTESIAN_POINT('Ctrl Pts',(0.0266020595922903,8.81,7.605));
#14303=CARTESIAN_POINT('Ctrl Pts',(-0.0266020595922903,8.81,7.605));
#14304=CARTESIAN_POINT('Ctrl Pts',(-0.0548298721325189,8.80463856105443,
7.6030741628997));
#14305=CARTESIAN_POINT('Ctrl Pts',(-0.100109787682299,8.78579931658744,
7.59698224789957));
#14306=CARTESIAN_POINT('Ctrl Pts',(-0.118254395260801,8.77472116821763,
7.59354677224418));
#14307=CARTESIAN_POINT('Ctrl Pts',(-0.133884278389955,8.76178689687364,
7.59));
#14308=CARTESIAN_POINT('Origin',(0.,8.6,7.59));
#14309=CARTESIAN_POINT('',(-0.133884278389956,8.2,7.59));
#14310=CARTESIAN_POINT('Origin',(0.,8.2,7.));
#14311=CARTESIAN_POINT('',(-0.605,9.,7.));
#14312=CARTESIAN_POINT('Origin',(0.,9.,7.));
#14313=CARTESIAN_POINT('',(-0.605,8.2,7.));
#14314=CARTESIAN_POINT('',(-0.605,8.2,7.));
#14315=CARTESIAN_POINT('Origin',(0.,8.2,7.));
#14316=CARTESIAN_POINT('Origin',(0.,8.2,7.));
#14317=CARTESIAN_POINT('',(-1.,9.,7.));
#14318=CARTESIAN_POINT('Origin',(0.,9.,7.));
#14319=CARTESIAN_POINT('',(-1.,8.2,7.));
#14320=CARTESIAN_POINT('',(-1.,8.2,7.));
#14321=CARTESIAN_POINT('Origin',(0.,8.2,7.));
#14322=CARTESIAN_POINT('Origin',(0.,9.,7.));
#14323=CARTESIAN_POINT('Origin',(0.,8.2,7.));
#14770=UNCERTAINTY_MEASURE_WITH_UNIT(LENGTH_MEASURE(0.001),#14823,
'DISTANCE_ACCURACY_VALUE',
'Maximum model space distance between geometric entities at asserted c
onnectivities');
#14777=UNCERTAINTY_MEASURE_WITH_UNIT(LENGTH_MEASURE(0.001),#14823,
'DISTANCE_ACCURACY_VALUE',
'Maximum model space distance between geometric entities at asserted c
onnectivities');
#14815=(
GEOMETRIC_REPRESENTATION_CONTEXT(3)
GLOBAL_UNCERTAINTY_ASSIGNED_CONTEXT((#14770))
GLOBAL_UNIT_ASSIGNED_CONTEXT((#14823,#14825,#14826))
REPRESENTATION_CONTEXT('','3D')
);
#14822=(
GEOMETRIC_REPRESENTATION_CONTEXT(3)
GLOBAL_UNCERTAINTY_ASSIGNED_CONTEXT((#14777))
GLOBAL_UNIT_ASSIGNED_CONTEXT((#14823,#14825,#14826))
REPRESENTATION_CONTEXT('','3D')
);
#14823=(
LENGTH_UNIT()
NAMED_UNIT(*)
SI_UNIT(.CENTI.,.METRE.)
);
#14825=(
NAMED_UNIT(*)
PLANE_ANGLE_UNIT()
SI_UNIT($,.RADIAN.)
);
#14826=(
NAMED_UNIT(*)
SI_UNIT($,.STERADIAN.)
SOLID_ANGLE_UNIT()
);
#14864=SHAPE_DEFINITION_REPRESENTATION(#14974,#15035);
#14974=PRODUCT_DEFINITION_SHAPE('',$,#15080);
#15035=SHAPE_REPRESENTATION('',(#9038),#14815);
#15042=PRODUCT_DEFINITION_CONTEXT('part definition',#15176,'design');
#15080=PRODUCT_DEFINITION('Journal collar (1)','Journal collar (1)',#15124,
#15042);
#15124=PRODUCT_DEFINITION_FORMATION('',$,#15215);
#15176=APPLICATION_CONTEXT(
'Core Data for Automotive Mechanical Design Process');
#15177=PRODUCT_CONTEXT('part definition',#15176,'mechanical');
#15215=PRODUCT('Journal collar (1)','Journal collar (1)','Journal collar (1)',
(#15177));
#15271=COLOUR_RGB('Sky Blue',0.24,0.69,0.87);
#15272=FILL_AREA_STYLE_COLOUR('',#15271);
#15273=FILL_AREA_STYLE('',(#15272));
#15274=SURFACE_STYLE_FILL_AREA(#15273);
#15275=SURFACE_SIDE_STYLE('',(#15274));
#15276=SURFACE_STYLE_USAGE(.BOTH.,#15275);
#15277=PRESENTATION_STYLE_ASSIGNMENT((#15276));
ENDSEC;
END-ISO-10303-21;
